ISO-10303-21;
HEADER;
/* Generated by software containing ST-Developer
 * from STEP Tools, Inc. (www.steptools.com) 
 */

FILE_DESCRIPTION(
/* description */ ('Four-bar parallelogram arm'),
/* implementation_level */ '2;1');

FILE_NAME(
/* name */ 'Pivot pin (2).step',
/* time_stamp */ '2026-10-28T03:24:55-07:00',
/* author */ (''),
/* organization */ (''),
/* preprocessor_version */ 'ST-DEVELOPER v20.2',
/* originating_system */ 'Autodesk Translation Framework v15.17.0.0',
/* authorisation */ '');

FILE_SCHEMA (('AUTOMOTIVE_DESIGN { 1 0 10303 214 3 1 1 }'));
ENDSEC;

DATA;
#10=MECHANICAL_DESIGN_GEOMETRIC_PRESENTATION_REPRESENTATION('',(#674),#14512);
#566=SHAPE_REPRESENTATION_RELATIONSHIP('SRR','None',#14791,#616);
#616=ADVANCED_BREP_SHAPE_REPRESENTATION('',(#730),#14506);
#674=STYLED_ITEM('',(#15087),#730);
#730=MANIFOLD_SOLID_BREP('Body1',#7380);
#988=FACE_BOUND('',#2255,.T.);
#989=FACE_BOUND('',#2256,.T.);
#990=FACE_BOUND('',#2257,.T.);
#991=FACE_BOUND('',#2258,.T.);
#992=FACE_BOUND('',#2260,.T.);
#993=FACE_BOUND('',#2261,.T.);
#994=FACE_BOUND('',#2262,.T.);
#995=FACE_BOUND('',#2263,.T.);
#996=FACE_BOUND('',#2269,.T.);
#1177=PLANE('',#8833);
#1178=PLANE('',#8843);
#1179=PLANE('',#8846);
#1180=PLANE('',#8854);
#1181=PLANE('',#8855);
#1576=FACE_OUTER_BOUND('',#2249,.T.);
#1577=FACE_OUTER_BOUND('',#2250,.T.);
#1578=FACE_OUTER_BOUND('',#2251,.T.);
#1579=FACE_OUTER_BOUND('',#2252,.T.);
#1580=FACE_OUTER_BOUND('',#2253,.T.);
#1581=FACE_OUTER_BOUND('',#2254,.T.);
#1582=FACE_OUTER_BOUND('',#2259,.T.);
#1583=FACE_OUTER_BOUND('',#2264,.T.);
#1584=FACE_OUTER_BOUND('',#2265,.T.);
#1585=FACE_OUTER_BOUND('',#2266,.T.);
#1586=FACE_OUTER_BOUND('',#2267,.T.);
#1587=FACE_OUTER_BOUND('',#2268,.T.);
#2249=EDGE_LOOP('',(#6560,#6561,#6562,#6563));
#2250=EDGE_LOOP('',(#6564));
#2251=EDGE_LOOP('',(#6565,#6566,#6567,#6568));
#2252=EDGE_LOOP('',(#6569,#6570,#6571,#6572));
#2253=EDGE_LOOP('',(#6573,#6574,#6575,#6576));
#2254=EDGE_LOOP('',(#6577));
#2255=EDGE_LOOP('',(#6578));
#2256=EDGE_LOOP('',(#6579));
#2257=EDGE_LOOP('',(#6580));
#2258=EDGE_LOOP('',(#6581));
#2259=EDGE_LOOP('',(#6582));
#2260=EDGE_LOOP('',(#6583));
#2261=EDGE_LOOP('',(#6584));
#2262=EDGE_LOOP('',(#6585));
#2263=EDGE_LOOP('',(#6586));
#2264=EDGE_LOOP('',(#6587,#6588,#6589,#6590));
#2265=EDGE_LOOP('',(#6591,#6592,#6593,#6594));
#2266=EDGE_LOOP('',(#6595,#6596,#6597,#6598));
#2267=EDGE_LOOP('',(#6599));
#2268=EDGE_LOOP('',(#6600));
#2269=EDGE_LOOP('',(#6601));
#2667=LINE('',#14174,#3061);
#2668=LINE('',#14181,#3062);
#2669=LINE('',#14187,#3063);
#2670=LINE('',#14193,#3064);
#2671=LINE('',#14206,#3065);
#2672=LINE('',#14209,#3066);
#2673=LINE('',#14214,#3067);
#3061=VECTOR('',#11113,0.164999999999999);
#3062=VECTOR('',#11122,0.225000000000001);
#3063=VECTOR('',#11129,0.225000000000001);
#3064=VECTOR('',#11136,0.225000000000001);
#3065=VECTOR('',#11153,1.5);
#3066=VECTOR('',#11156,0.5);
#3067=VECTOR('',#11163,0.5);
#3507=CIRCLE('',#8831,0.164999999999999);
#3508=CIRCLE('',#8832,0.164999999999999);
#3509=CIRCLE('',#8835,0.225000000000001);
#3510=CIRCLE('',#8836,0.225000000000001);
#3511=CIRCLE('',#8838,0.225000000000001);
#3512=CIRCLE('',#8839,0.225000000000001);
#3513=CIRCLE('',#8841,0.225000000000001);
#3514=CIRCLE('',#8842,0.225000000000001);
#3515=CIRCLE('',#8844,1.5);
#3516=CIRCLE('',#8845,0.5);
#3517=CIRCLE('',#8847,1.5);
#3518=CIRCLE('',#8848,0.5);
#3519=CIRCLE('',#8851,0.5);
#3520=CIRCLE('',#8853,0.5);
#4075=VERTEX_POINT('',#14171);
#4076=VERTEX_POINT('',#14173);
#4077=VERTEX_POINT('',#14178);
#4078=VERTEX_POINT('',#14180);
#4079=VERTEX_POINT('',#14184);
#4080=VERTEX_POINT('',#14186);
#4081=VERTEX_POINT('',#14190);
#4082=VERTEX_POINT('',#14192);
#4083=VERTEX_POINT('',#14196);
#4084=VERTEX_POINT('',#14198);
#4085=VERTEX_POINT('',#14201);
#4086=VERTEX_POINT('',#14203);
#4087=VERTEX_POINT('',#14208);
#4088=VERTEX_POINT('',#14212);
#4911=EDGE_CURVE('',#4075,#4075,#3507,.T.);
#4912=EDGE_CURVE('',#4075,#4076,#2667,.T.);
#4913=EDGE_CURVE('',#4076,#4076,#3508,.T.);
#4914=EDGE_CURVE('',#4077,#4077,#3509,.T.);
#4915=EDGE_CURVE('',#4077,#4078,#2668,.T.);
#4916=EDGE_CURVE('',#4078,#4078,#3510,.T.);
#4917=EDGE_CURVE('',#4079,#4079,#3511,.T.);
#4918=EDGE_CURVE('',#4079,#4080,#2669,.T.);
#4919=EDGE_CURVE('',#4080,#4080,#3512,.T.);
#4920=EDGE_CURVE('',#4081,#4081,#3513,.T.);
#4921=EDGE_CURVE('',#4081,#4082,#2670,.T.);
#4922=EDGE_CURVE('',#4082,#4082,#3514,.T.);
#4923=EDGE_CURVE('',#4083,#4083,#3515,.T.);
#4924=EDGE_CURVE('',#4084,#4084,#3516,.T.);
#4925=EDGE_CURVE('',#4085,#4085,#3517,.T.);
#4926=EDGE_CURVE('',#4086,#4086,#3518,.T.);
#4927=EDGE_CURVE('',#4083,#4085,#2671,.T.);
#4928=EDGE_CURVE('',#4086,#4087,#2672,.T.);
#4929=EDGE_CURVE('',#4087,#4087,#3519,.T.);
#4930=EDGE_CURVE('',#4088,#4088,#3520,.T.);
#4931=EDGE_CURVE('',#4088,#4084,#2673,.T.);
#6560=ORIENTED_EDGE('',*,*,#4911,.F.);
#6561=ORIENTED_EDGE('',*,*,#4912,.T.);
#6562=ORIENTED_EDGE('',*,*,#4913,.T.);
#6563=ORIENTED_EDGE('',*,*,#4912,.F.);
#6564=ORIENTED_EDGE('',*,*,#4913,.F.);
#6565=ORIENTED_EDGE('',*,*,#4914,.F.);
#6566=ORIENTED_EDGE('',*,*,#4915,.T.);
#6567=ORIENTED_EDGE('',*,*,#4916,.F.);
#6568=ORIENTED_EDGE('',*,*,#4915,.F.);
#6569=ORIENTED_EDGE('',*,*,#4917,.F.);
#6570=ORIENTED_EDGE('',*,*,#4918,.T.);
#6571=ORIENTED_EDGE('',*,*,#4919,.F.);
#6572=ORIENTED_EDGE('',*,*,#4918,.F.);
#6573=ORIENTED_EDGE('',*,*,#4920,.F.);
#6574=ORIENTED_EDGE('',*,*,#4921,.T.);
#6575=ORIENTED_EDGE('',*,*,#4922,.F.);
#6576=ORIENTED_EDGE('',*,*,#4921,.F.);
#6577=ORIENTED_EDGE('',*,*,#4923,.T.);
#6578=ORIENTED_EDGE('',*,*,#4916,.T.);
#6579=ORIENTED_EDGE('',*,*,#4919,.T.);
#6580=ORIENTED_EDGE('',*,*,#4922,.T.);
#6581=ORIENTED_EDGE('',*,*,#4924,.F.);
#6582=ORIENTED_EDGE('',*,*,#4925,.F.);
#6583=ORIENTED_EDGE('',*,*,#4914,.T.);
#6584=ORIENTED_EDGE('',*,*,#4917,.T.);
#6585=ORIENTED_EDGE('',*,*,#4920,.T.);
#6586=ORIENTED_EDGE('',*,*,#4926,.F.);
#6587=ORIENTED_EDGE('',*,*,#4923,.F.);
#6588=ORIENTED_EDGE('',*,*,#4927,.T.);
#6589=ORIENTED_EDGE('',*,*,#4925,.T.);
#6590=ORIENTED_EDGE('',*,*,#4927,.F.);
#6591=ORIENTED_EDGE('',*,*,#4926,.T.);
#6592=ORIENTED_EDGE('',*,*,#4928,.T.);
#6593=ORIENTED_EDGE('',*,*,#4929,.T.);
#6594=ORIENTED_EDGE('',*,*,#4928,.F.);
#6595=ORIENTED_EDGE('',*,*,#4930,.F.);
#6596=ORIENTED_EDGE('',*,*,#4931,.T.);
#6597=ORIENTED_EDGE('',*,*,#4924,.T.);
#6598=ORIENTED_EDGE('',*,*,#4931,.F.);
#6599=ORIENTED_EDGE('',*,*,#4930,.T.);
#6600=ORIENTED_EDGE('',*,*,#4929,.F.);
#6601=ORIENTED_EDGE('',*,*,#4911,.T.);
#6889=CYLINDRICAL_SURFACE('',#8830,0.164999999999999);
#6890=CYLINDRICAL_SURFACE('',#8834,0.225000000000001);
#6891=CYLINDRICAL_SURFACE('',#8837,0.225000000000001);
#6892=CYLINDRICAL_SURFACE('',#8840,0.225000000000001);
#6893=CYLINDRICAL_SURFACE('',#8849,1.5);
#6894=CYLINDRICAL_SURFACE('',#8850,0.5);
#6895=CYLINDRICAL_SURFACE('',#8852,0.5);
#7281=ADVANCED_FACE('',(#1576),#6889,.F.);
#7282=ADVANCED_FACE('',(#1577),#1177,.F.);
#7283=ADVANCED_FACE('',(#1578),#6890,.F.);
#7284=ADVANCED_FACE('',(#1579),#6891,.F.);
#7285=ADVANCED_FACE('',(#1580),#6892,.F.);
#7286=ADVANCED_FACE('',(#1581,#988,#989,#990,#991),#1178,.T.);
#7287=ADVANCED_FACE('',(#1582,#992,#993,#994,#995),#1179,.F.);
#7288=ADVANCED_FACE('',(#1583),#6893,.T.);
#7289=ADVANCED_FACE('',(#1584),#6894,.T.);
#7290=ADVANCED_FACE('',(#1585),#6895,.T.);
#7291=ADVANCED_FACE('',(#1586),#1180,.T.);
#7292=ADVANCED_FACE('',(#1587,#996),#1181,.F.);
#7380=CLOSED_SHELL('',(#7281,#7282,#7283,#7284,#7285,#7286,#7287,#7288,
#7289,#7290,#7291,#7292));
#8829=AXIS2_PLACEMENT_3D('',#14169,#11107,#11108);
#8830=AXIS2_PLACEMENT_3D('',#14170,#11109,#11110);
#8831=AXIS2_PLACEMENT_3D('',#14172,#11111,#11112);
#8832=AXIS2_PLACEMENT_3D('',#14175,#11114,#11115);
#8833=AXIS2_PLACEMENT_3D('',#14176,#11116,#11117);
#8834=AXIS2_PLACEMENT_3D('',#14177,#11118,#11119);
#8835=AXIS2_PLACEMENT_3D('',#14179,#11120,#11121);
#8836=AXIS2_PLACEMENT_3D('',#14182,#11123,#11124);
#8837=AXIS2_PLACEMENT_3D('',#14183,#11125,#11126);
#8838=AXIS2_PLACEMENT_3D('',#14185,#11127,#11128);
#8839=AXIS2_PLACEMENT_3D('',#14188,#11130,#11131);
#8840=AXIS2_PLACEMENT_3D('',#14189,#11132,#11133);
#8841=AXIS2_PLACEMENT_3D('',#14191,#11134,#11135);
#8842=AXIS2_PLACEMENT_3D('',#14194,#11137,#11138);
#8843=AXIS2_PLACEMENT_3D('',#14195,#11139,#11140);
#8844=AXIS2_PLACEMENT_3D('',#14197,#11141,#11142);
#8845=AXIS2_PLACEMENT_3D('',#14199,#11143,#11144);
#8846=AXIS2_PLACEMENT_3D('',#14200,#11145,#11146);
#8847=AXIS2_PLACEMENT_3D('',#14202,#11147,#11148);
#8848=AXIS2_PLACEMENT_3D('',#14204,#11149,#11150);
#8849=AXIS2_PLACEMENT_3D('',#14205,#11151,#11152);
#8850=AXIS2_PLACEMENT_3D('',#14207,#11154,#11155);
#8851=AXIS2_PLACEMENT_3D('',#14210,#11157,#11158);
#8852=AXIS2_PLACEMENT_3D('',#14211,#11159,#11160);
#8853=AXIS2_PLACEMENT_3D('',#14213,#11161,#11162);
#8854=AXIS2_PLACEMENT_3D('',#14215,#11164,#11165);
#8855=AXIS2_PLACEMENT_3D('',#14216,#11166,#11167);
#11107=DIRECTION('axis',(0.,0.,1.));
#11108=DIRECTION('refdir',(1.,0.,0.));
#11109=DIRECTION('center_axis',(0.,1.,0.));
#11110=DIRECTION('ref_axis',(1.,0.,0.));
#11111=DIRECTION('center_axis',(0.,1.,0.));
#11112=DIRECTION('ref_axis',(1.,0.,0.));
#11113=DIRECTION('',(0.,1.,0.));
#11114=DIRECTION('center_axis',(0.,1.,0.));
#11115=DIRECTION('ref_axis',(1.,0.,0.));
#11116=DIRECTION('center_axis',(0.,1.,0.));
#11117=DIRECTION('ref_axis',(1.,0.,0.));
#11118=DIRECTION('center_axis',(0.,1.,0.));
#11119=DIRECTION('ref_axis',(1.,0.,0.));
#11120=DIRECTION('center_axis',(0.,1.,0.));
#11121=DIRECTION('ref_axis',(1.,0.,0.));
#11122=DIRECTION('',(0.,1.,0.));
#11123=DIRECTION('center_axis',(0.,-1.,0.));
#11124=DIRECTION('ref_axis',(1.,0.,0.));
#11125=DIRECTION('center_axis',(0.,1.,0.));
#11126=DIRECTION('ref_axis',(1.,0.,0.));
#11127=DIRECTION('center_axis',(0.,1.,0.));
#11128=DIRECTION('ref_axis',(1.,0.,0.));
#11129=DIRECTION('',(0.,1.,0.));
#11130=DIRECTION('center_axis',(0.,-1.,0.));
#11131=DIRECTION('ref_axis',(1.,0.,0.));
#11132=DIRECTION('center_axis',(0.,1.,0.));
#11133=DIRECTION('ref_axis',(1.,0.,0.));
#11134=DIRECTION('center_axis',(0.,1.,0.));
#11135=DIRECTION('ref_axis',(1.,0.,0.));
#11136=DIRECTION('',(0.,1.,0.));
#11137=DIRECTION('center_axis',(0.,-1.,0.));
#11138=DIRECTION('ref_axis',(1.,0.,0.));
#11139=DIRECTION('center_axis',(0.,1.,0.));
#11140=DIRECTION('ref_axis',(1.,0.,0.));
#11141=DIRECTION('center_axis',(0.,1.,0.));
#11142=DIRECTION('ref_axis',(1.,0.,0.));
#11143=DIRECTION('center_axis',(0.,1.,0.));
#11144=DIRECTION('ref_axis',(1.,0.,0.));
#11145=DIRECTION('center_axis',(0.,1.,0.));
#11146=DIRECTION('ref_axis',(1.,0.,0.));
#11147=DIRECTION('center_axis',(0.,1.,0.));
#11148=DIRECTION('ref_axis',(1.,0.,0.));
#11149=DIRECTION('center_axis',(0.,-1.,0.));
#11150=DIRECTION('ref_axis',(1.,0.,0.));
#11151=DIRECTION('center_axis',(0.,1.,0.));
#11152=DIRECTION('ref_axis',(1.,0.,0.));
#11153=DIRECTION('',(0.,-1.,0.));
#11154=DIRECTION('center_axis',(0.,1.,0.));
#11155=DIRECTION('ref_axis',(1.,0.,0.));
#11156=DIRECTION('',(0.,-1.,0.));
#11157=DIRECTION('center_axis',(0.,1.,0.));
#11158=DIRECTION('ref_axis',(1.,0.,0.));
#11159=DIRECTION('center_axis',(0.,1.,0.));
#11160=DIRECTION('ref_axis',(1.,0.,0.));
#11161=DIRECTION('center_axis',(0.,1.,0.));
#11162=DIRECTION('ref_axis',(1.,0.,0.));
#11163=DIRECTION('',(0.,-1.,0.));
#11164=DIRECTION('center_axis',(0.,1.,0.));
#11165=DIRECTION('ref_axis',(1.,0.,0.));
#11166=DIRECTION('center_axis',(0.,1.,0.));
#11167=DIRECTION('ref_axis',(1.,0.,0.));
#14169=CARTESIAN_POINT('',(0.,0.,0.));
#14170=CARTESIAN_POINT('Origin',(20.,-1.7,14.));
#14171=CARTESIAN_POINT('',(19.835,-1.6,14.));
#14172=CARTESIAN_POINT('Origin',(20.,-1.6,14.));
#14173=CARTESIAN_POINT('',(19.835,0.,14.));
#14174=CARTESIAN_POINT('',(19.835,-1.7,14.));
#14175=CARTESIAN_POINT('Origin',(20.,0.,14.));
#14176=CARTESIAN_POINT('Origin',(20.,0.,14.));
#14177=CARTESIAN_POINT('Origin',(21.15,2.4,14.));
#14178=CARTESIAN_POINT('',(20.925,2.5,14.));
#14179=CARTESIAN_POINT('Origin',(21.15,2.5,14.));
#14180=CARTESIAN_POINT('',(20.925,2.9,14.));
#14181=CARTESIAN_POINT('',(20.925,2.4,14.));
#14182=CARTESIAN_POINT('Origin',(21.15,2.9,14.));
#14183=CARTESIAN_POINT('Origin',(19.425,2.4,14.9959292143521));
#14184=CARTESIAN_POINT('',(19.2,2.5,14.9959292143521));
#14185=CARTESIAN_POINT('Origin',(19.425,2.5,14.9959292143521));
#14186=CARTESIAN_POINT('',(19.2,2.9,14.9959292143521));
#14187=CARTESIAN_POINT('',(19.2,2.4,14.9959292143521));
#14188=CARTESIAN_POINT('Origin',(19.425,2.9,14.9959292143521));
#14189=CARTESIAN_POINT('Origin',(19.425,2.4,13.0040707856479));
#14190=CARTESIAN_POINT('',(19.2,2.5,13.0040707856479));
#14191=CARTESIAN_POINT('Origin',(19.425,2.5,13.0040707856479));
#14192=CARTESIAN_POINT('',(19.2,2.9,13.0040707856479));
#14193=CARTESIAN_POINT('',(19.2,2.4,13.0040707856479));
#14194=CARTESIAN_POINT('Origin',(19.425,2.9,13.0040707856479));
#14195=CARTESIAN_POINT('Origin',(20.,2.9,14.));
#14196=CARTESIAN_POINT('',(18.5,2.9,14.));
#14197=CARTESIAN_POINT('Origin',(20.,2.9,14.));
#14198=CARTESIAN_POINT('',(19.5,2.9,14.));
#14199=CARTESIAN_POINT('Origin',(20.,2.9,14.));
#14200=CARTESIAN_POINT('Origin',(20.,2.5,14.));
#14201=CARTESIAN_POINT('',(18.5,2.5,14.));
#14202=CARTESIAN_POINT('Origin',(20.,2.5,14.));
#14203=CARTESIAN_POINT('',(19.5,2.5,14.));
#14204=CARTESIAN_POINT('Origin',(20.,2.5,14.));
#14205=CARTESIAN_POINT('Origin',(20.,2.5,14.));
#14206=CARTESIAN_POINT('',(18.5,2.5,14.));
#14207=CARTESIAN_POINT('Origin',(20.,-1.6,14.));
#14208=CARTESIAN_POINT('',(19.5,-1.6,14.));
#14209=CARTESIAN_POINT('',(19.5,-1.6,14.));
#14210=CARTESIAN_POINT('Origin',(20.,-1.6,14.));
#14211=CARTESIAN_POINT('Origin',(20.,-1.6,14.));
#14212=CARTESIAN_POINT('',(19.5,3.9,14.));
#14213=CARTESIAN_POINT('Origin',(20.,3.9,14.));
#14214=CARTESIAN_POINT('',(19.5,-1.6,14.));
#14215=CARTESIAN_POINT('Origin',(20.,3.9,14.));
#14216=CARTESIAN_POINT('Origin',(20.,-1.6,14.));
#14449=UNCERTAINTY_MEASURE_WITH_UNIT(LENGTH_MEASURE(0.001),#14513,
'DISTANCE_ACCURACY_VALUE',
'Maximum model space distance between geometric entities at asserted c
onnectivities');
#14455=UNCERTAINTY_MEASURE_WITH_UNIT(LENGTH_MEASURE(0.001),#14513,
'DISTANCE_ACCURACY_VALUE',
'Maximum model space distance between geometric entities at asserted c
onnectivities');
#14506=(
GEOMETRIC_REPRESENTATION_CONTEXT(3)
GLOBAL_UNCERTAINTY_ASSIGNED_CONTEXT((#14449))
GLOBAL_UNIT_ASSIGNED_CONTEXT((#14513,#14515,#14516))
REPRESENTATION_CONTEXT('','3D')
);
#14512=(
GEOMETRIC_REPRESENTATION_CONTEXT(3)
GLOBAL_UNCERTAINTY_ASSIGNED_CONTEXT((#14455))
GLOBAL_UNIT_ASSIGNED_CONTEXT((#14513,#14515,#14516))
REPRESENTATION_CONTEXT('','3D')
);
#14513=(
LENGTH_UNIT()
NAMED_UNIT(*)
SI_UNIT(.CENTI.,.METRE.)
);
#14515=(
NAMED_UNIT(*)
PLANE_ANGLE_UNIT()
SI_UNIT($,.RADIAN.)
);
#14516=(
NAMED_UNIT(*)
SI_UNIT($,.STERADIAN.)
SOLID_ANGLE_UNIT()
);
#14567=SHAPE_DEFINITION_REPRESENTATION(#14683,#14791);
#14683=PRODUCT_DEFINITION_SHAPE('',$,#14848);
#14791=SHAPE_REPRESENTATION('',(#8829),#14506);
#14797=PRODUCT_DEFINITION_CONTEXT('part definition',#14967,'design');
#14848=PRODUCT_DEFINITION('Pivot pin (2)','Pivot pin (2)',#14904,#14797);
#14904=PRODUCT_DEFINITION_FORMATION('',$,#15019);
#14967=APPLICATION_CONTEXT(
'Core Data for Automotive Mechanical Design Process');
#14968=PRODUCT_CONTEXT('part definition',#14967,'mechanical');
#15019=PRODUCT('Pivot pin (2)','Pivot pin (2)','Pivot pin (2)',(#14968));
#15081=COLOUR_RGB('Grey',0.48,0.52,0.57);
#15082=FILL_AREA_STYLE_COLOUR('',#15081);
#15083=FILL_AREA_STYLE('',(#15082));
#15084=SURFACE_STYLE_FILL_AREA(#15083);
#15085=SURFACE_SIDE_STYLE('',(#15084));
#15086=SURFACE_STYLE_USAGE(.BOTH.,#15085);
#15087=PRESENTATION_STYLE_ASSIGNMENT((#15086));
ENDSEC;
END-ISO-10303-21;
